ISO-10303-21;
HEADER;
/* Generated by software containing ST-Developer
 * from STEP Tools, Inc. (www.steptools.com) 
 */

FILE_DESCRIPTION(
/* description */ (''),
/* implementation_level */ '2;1');

FILE_NAME(
/* name */ 'Rod.step',
/* time_stamp */ '2026-10-19T02:00:06+06:00',
/* author */ (''),
/* organization */ (''),
/* preprocessor_version */ 'ST-DEVELOPER v20.2',
/* originating_system */ 'Autodesk Translation Framework v15.15.0.0',
/* authorisation */ '');

FILE_SCHEMA (('AUTOMOTIVE_DESIGN { 1 0 10303 214 3 1 1 }'));
ENDSEC;

DATA;
#10=MECHANICAL_DESIGN_GEOMETRIC_PRESENTATION_REPRESENTATION('',(#107),#4833);
#85=SHAPE_REPRESENTATION_RELATIONSHIP('SRR','None',#4876,#96);
#96=ADVANCED_BREP_SHAPE_REPRESENTATION('',(#118),#4824);
#107=STYLED_ITEM('',(#4992),#118);
#118=MANIFOLD_SOLID_BREP('Rod',#2689);
#188=PLANE('',#2887);
#189=PLANE('',#2888);
#304=FACE_OUTER_BOUND('',#477,.T.);
#305=FACE_OUTER_BOUND('',#478,.T.);
#306=FACE_OUTER_BOUND('',#479,.T.);
#477=EDGE_LOOP('',(#1897,#1898,#1899,#1900));
#478=EDGE_LOOP('',(#1901));
#479=EDGE_LOOP('',(#1902));
#663=LINE('',#4028,#917);
#917=VECTOR('',#3258,6.);
#1159=CIRCLE('',#2885,6.);
#1160=CIRCLE('',#2886,6.);
#1245=VERTEX_POINT('',#4025);
#1246=VERTEX_POINT('',#4027);
#1489=EDGE_CURVE('',#1245,#1245,#1159,.T.);
#1490=EDGE_CURVE('',#1245,#1246,#663,.T.);
#1491=EDGE_CURVE('',#1246,#1246,#1160,.T.);
#1897=ORIENTED_EDGE('',*,*,#1489,.F.);
#1898=ORIENTED_EDGE('',*,*,#1490,.T.);
#1899=ORIENTED_EDGE('',*,*,#1491,.T.);
#1900=ORIENTED_EDGE('',*,*,#1490,.F.);
#1901=ORIENTED_EDGE('',*,*,#1489,.T.);
#1902=ORIENTED_EDGE('',*,*,#1491,.F.);
#2485=CYLINDRICAL_SURFACE('',#2884,6.);
#2562=ADVANCED_FACE('',(#304),#2485,.T.);
#2563=ADVANCED_FACE('',(#305),#188,.T.);
#2564=ADVANCED_FACE('',(#306),#189,.F.);
#2689=CLOSED_SHELL('',(#2562,#2563,#2564));
#2883=AXIS2_PLACEMENT_3D('',#4023,#3252,#3253);
#2884=AXIS2_PLACEMENT_3D('',#4024,#3254,#3255);
#2885=AXIS2_PLACEMENT_3D('',#4026,#3256,#3257);
#2886=AXIS2_PLACEMENT_3D('',#4029,#3259,#3260);
#2887=AXIS2_PLACEMENT_3D('',#4030,#3261,#3262);
#2888=AXIS2_PLACEMENT_3D('',#4031,#3263,#3264);
#3252=DIRECTION('axis',(0.,0.,1.));
#3253=DIRECTION('refdir',(1.,0.,0.));
#3254=DIRECTION('center_axis',(-1.,0.,0.));
#3255=DIRECTION('ref_axis',(0.,-1.,0.));
#3256=DIRECTION('center_axis',(-1.,0.,0.));
#3257=DIRECTION('ref_axis',(0.,-1.,0.));
#3258=DIRECTION('',(1.,0.,0.));
#3259=DIRECTION('center_axis',(-1.,0.,0.));
#3260=DIRECTION('ref_axis',(0.,-1.,0.));
#3261=DIRECTION('center_axis',(-1.,0.,0.));
#3262=DIRECTION('ref_axis',(0.,-1.,0.));
#3263=DIRECTION('center_axis',(-1.,0.,0.));
#3264=DIRECTION('ref_axis',(0.,-1.,0.));
#4023=CARTESIAN_POINT('',(0.,0.,0.));
#4024=CARTESIAN_POINT('Origin',(70.,-30.0000000000105,7.00000000000211));
#4025=CARTESIAN_POINT('',(-90.,-24.0000000000105,7.00000000000211));
#4026=CARTESIAN_POINT('Origin',(-90.,-30.0000000000105,7.00000000000211));
#4027=CARTESIAN_POINT('',(70.,-24.0000000000105,7.00000000000211));
#4028=CARTESIAN_POINT('',(70.,-24.0000000000105,7.00000000000211));
#4029=CARTESIAN_POINT('Origin',(70.,-30.0000000000105,7.00000000000211));
#4030=CARTESIAN_POINT('Origin',(-90.,-30.0000000000105,7.00000000000211));
#4031=CARTESIAN_POINT('Origin',(70.,-30.0000000000105,7.00000000000211));
#4811=UNCERTAINTY_MEASURE_WITH_UNIT(LENGTH_MEASURE(0.01),#4834,
'DISTANCE_ACCURACY_VALUE',
'Maximum model space distance between geometric entities at asserted c
onnectivities');
#4820=UNCERTAINTY_MEASURE_WITH_UNIT(LENGTH_MEASURE(0.01),#4834,
'DISTANCE_ACCURACY_VALUE',
'Maximum model space distance between geometric entities at asserted c
onnectivities');
#4824=(
GEOMETRIC_REPRESENTATION_CONTEXT(3)
GLOBAL_UNCERTAINTY_ASSIGNED_CONTEXT((#4811))
GLOBAL_UNIT_ASSIGNED_CONTEXT((#4834,#4836,#4837))
REPRESENTATION_CONTEXT('','3D')
);
#4833=(
GEOMETRIC_REPRESENTATION_CONTEXT(3)
GLOBAL_UNCERTAINTY_ASSIGNED_CONTEXT((#4820))
GLOBAL_UNIT_ASSIGNED_CONTEXT((#4834,#4836,#4837))
REPRESENTATION_CONTEXT('','3D')
);
#4834=(
LENGTH_UNIT()
NAMED_UNIT(*)
SI_UNIT(.MILLI.,.METRE.)
);
#4836=(
NAMED_UNIT(*)
PLANE_ANGLE_UNIT()
SI_UNIT($,.RADIAN.)
);
#4837=(
NAMED_UNIT(*)
SI_UNIT($,.STERADIAN.)
SOLID_ANGLE_UNIT()
);
#4841=SHAPE_DEFINITION_REPRESENTATION(#4853,#4876);
#4853=PRODUCT_DEFINITION_SHAPE('',$,#4889);
#4876=SHAPE_REPRESENTATION('',(#2883),#4824);
#4885=PRODUCT_DEFINITION_CONTEXT('part definition',#4923,'design');
#4889=PRODUCT_DEFINITION('Rod','Rod',#4901,#4885);
#4901=PRODUCT_DEFINITION_FORMATION('',$,#4928);
#4923=APPLICATION_CONTEXT(
'Core Data for Automotive Mechanical Design Process');
#4924=PRODUCT_CONTEXT('part definition',#4923,'mechanical');
#4928=PRODUCT('Rod','Rod',$,(#4924));
#4986=COLOUR_RGB('Grey',0.48,0.52,0.57);
#4987=FILL_AREA_STYLE_COLOUR('',#4986);
#4988=FILL_AREA_STYLE('',(#4987));
#4989=SURFACE_STYLE_FILL_AREA(#4988);
#4990=SURFACE_SIDE_STYLE('',(#4989));
#4991=SURFACE_STYLE_USAGE(.BOTH.,#4990);
#4992=PRESENTATION_STYLE_ASSIGNMENT((#4991));
ENDSEC;
END-ISO-10303-21;
